ISO-10303-21;
HEADER;
/* Generated by software containing ST-Developer
 * from STEP Tools, Inc. (www.steptools.com) 
 */

FILE_DESCRIPTION(
/* description */ ('Turntable on roller ring'),
/* implementation_level */ '2;1');

FILE_NAME(
/* name */ 'Roller axle (1).step',
/* time_stamp */ '2026-10-28T03:23:59-07:00',
/* author */ (''),
/* organization */ (''),
/* preprocessor_version */ 'ST-DEVELOPER v20.2',
/* originating_system */ 'Autodesk Translation Framework v15.17.0.0',
/* authorisation */ '');

FILE_SCHEMA (('AUTOMOTIVE_DESIGN { 1 0 10303 214 3 1 1 }'));
ENDSEC;

DATA;
#10=MECHANICAL_DESIGN_GEOMETRIC_PRESENTATION_REPRESENTATION('',(#648),#16281);
#529=SHAPE_REPRESENTATION_RELATIONSHIP('SRR','None',#16547,#584);
#584=ADVANCED_BREP_SHAPE_REPRESENTATION('',(#718),#16241);
#648=STYLED_ITEM('',(#16932),#718);
#718=MANIFOLD_SOLID_BREP('Body1',#8391);
#903=FACE_BOUND('',#2177,.T.);
#904=FACE_BOUND('',#2182,.T.);
#1125=PLANE('',#9649);
#1126=PLANE('',#9650);
#1127=PLANE('',#9655);
#1128=PLANE('',#9658);
#1523=FACE_OUTER_BOUND('',#2174,.T.);
#1524=FACE_OUTER_BOUND('',#2175,.T.);
#1525=FACE_OUTER_BOUND('',#2176,.T.);
#1526=FACE_OUTER_BOUND('',#2178,.T.);
#1527=FACE_OUTER_BOUND('',#2179,.T.);
#1528=FACE_OUTER_BOUND('',#2180,.T.);
#1529=FACE_OUTER_BOUND('',#2181,.T.);
#2174=EDGE_LOOP('',(#6815,#6816,#6817,#6818));
#2175=EDGE_LOOP('',(#6819));
#2176=EDGE_LOOP('',(#6820));
#2177=EDGE_LOOP('',(#6821));
#2178=EDGE_LOOP('',(#6822,#6823,#6824,#6825));
#2179=EDGE_LOOP('',(#6826));
#2180=EDGE_LOOP('',(#6827,#6828,#6829,#6830));
#2181=EDGE_LOOP('',(#6831));
#2182=EDGE_LOOP('',(#6832));
#2779=LINE('',#14749,#3262);
#2780=LINE('',#14759,#3263);
#2781=LINE('',#14765,#3264);
#3262=VECTOR('',#11702,0.165);
#3263=VECTOR('',#11715,0.8);
#3264=VECTOR('',#11724,0.5);
#3737=CIRCLE('',#9647,0.165);
#3738=CIRCLE('',#9648,0.165);
#3739=CIRCLE('',#9651,0.8);
#3740=CIRCLE('',#9652,0.5);
#3741=CIRCLE('',#9654,0.8);
#3742=CIRCLE('',#9657,0.5);
#4341=VERTEX_POINT('',#14746);
#4342=VERTEX_POINT('',#14748);
#4343=VERTEX_POINT('',#14753);
#4344=VERTEX_POINT('',#14755);
#4345=VERTEX_POINT('',#14758);
#4346=VERTEX_POINT('',#14763);
#5218=EDGE_CURVE('',#4341,#4341,#3737,.T.);
#5219=EDGE_CURVE('',#4341,#4342,#2779,.T.);
#5220=EDGE_CURVE('',#4342,#4342,#3738,.T.);
#5221=EDGE_CURVE('',#4343,#4343,#3739,.T.);
#5222=EDGE_CURVE('',#4344,#4344,#3740,.T.);
#5223=EDGE_CURVE('',#4343,#4345,#2780,.T.);
#5224=EDGE_CURVE('',#4345,#4345,#3741,.T.);
#5225=EDGE_CURVE('',#4346,#4346,#3742,.T.);
#5226=EDGE_CURVE('',#4346,#4344,#2781,.T.);
#6815=ORIENTED_EDGE('',*,*,#5218,.F.);
#6816=ORIENTED_EDGE('',*,*,#5219,.T.);
#6817=ORIENTED_EDGE('',*,*,#5220,.F.);
#6818=ORIENTED_EDGE('',*,*,#5219,.F.);
#6819=ORIENTED_EDGE('',*,*,#5218,.T.);
#6820=ORIENTED_EDGE('',*,*,#5221,.T.);
#6821=ORIENTED_EDGE('',*,*,#5222,.F.);
#6822=ORIENTED_EDGE('',*,*,#5221,.F.);
#6823=ORIENTED_EDGE('',*,*,#5223,.T.);
#6824=ORIENTED_EDGE('',*,*,#5224,.T.);
#6825=ORIENTED_EDGE('',*,*,#5223,.F.);
#6826=ORIENTED_EDGE('',*,*,#5224,.F.);
#6827=ORIENTED_EDGE('',*,*,#5225,.F.);
#6828=ORIENTED_EDGE('',*,*,#5226,.T.);
#6829=ORIENTED_EDGE('',*,*,#5222,.T.);
#6830=ORIENTED_EDGE('',*,*,#5226,.F.);
#6831=ORIENTED_EDGE('',*,*,#5225,.T.);
#6832=ORIENTED_EDGE('',*,*,#5220,.T.);
#7774=CYLINDRICAL_SURFACE('',#9646,0.165);
#7775=CYLINDRICAL_SURFACE('',#9653,0.8);
#7776=CYLINDRICAL_SURFACE('',#9656,0.5);
#8126=ADVANCED_FACE('',(#1523),#7774,.F.);
#8127=ADVANCED_FACE('',(#1524),#1125,.T.);
#8128=ADVANCED_FACE('',(#1525,#903),#1126,.T.);
#8129=ADVANCED_FACE('',(#1526),#7775,.T.);
#8130=ADVANCED_FACE('',(#1527),#1127,.F.);
#8131=ADVANCED_FACE('',(#1528),#7776,.T.);
#8132=ADVANCED_FACE('',(#1529,#904),#1128,.T.);
#8391=CLOSED_SHELL('',(#8126,#8127,#8128,#8129,#8130,#8131,#8132));
#9645=AXIS2_PLACEMENT_3D('',#14744,#11696,#11697);
#9646=AXIS2_PLACEMENT_3D('',#14745,#11698,#11699);
#9647=AXIS2_PLACEMENT_3D('',#14747,#11700,#11701);
#9648=AXIS2_PLACEMENT_3D('',#14750,#11703,#11704);
#9649=AXIS2_PLACEMENT_3D('',#14751,#11705,#11706);
#9650=AXIS2_PLACEMENT_3D('',#14752,#11707,#11708);
#9651=AXIS2_PLACEMENT_3D('',#14754,#11709,#11710);
#9652=AXIS2_PLACEMENT_3D('',#14756,#11711,#11712);
#9653=AXIS2_PLACEMENT_3D('',#14757,#11713,#11714);
#9654=AXIS2_PLACEMENT_3D('',#14760,#11716,#11717);
#9655=AXIS2_PLACEMENT_3D('',#14761,#11718,#11719);
#9656=AXIS2_PLACEMENT_3D('',#14762,#11720,#11721);
#9657=AXIS2_PLACEMENT_3D('',#14764,#11722,#11723);
#9658=AXIS2_PLACEMENT_3D('',#14766,#11725,#11726);
#11696=DIRECTION('axis',(0.,0.,1.));
#11697=DIRECTION('refdir',(1.,0.,0.));
#11698=DIRECTION('center_axis',(0.,1.,0.));
#11699=DIRECTION('ref_axis',(1.,0.,0.));
#11700=DIRECTION('center_axis',(0.,1.,0.));
#11701=DIRECTION('ref_axis',(1.,0.,0.));
#11702=DIRECTION('',(0.,1.,0.));
#11703=DIRECTION('center_axis',(0.,-1.,0.));
#11704=DIRECTION('ref_axis',(1.,0.,0.));
#11705=DIRECTION('center_axis',(0.,1.,0.));
#11706=DIRECTION('ref_axis',(1.,0.,0.));
#11707=DIRECTION('center_axis',(0.,1.,0.));
#11708=DIRECTION('ref_axis',(1.,0.,0.));
#11709=DIRECTION('center_axis',(0.,1.,0.));
#11710=DIRECTION('ref_axis',(1.,0.,0.));
#11711=DIRECTION('center_axis',(0.,1.,0.));
#11712=DIRECTION('ref_axis',(1.,0.,0.));
#11713=DIRECTION('center_axis',(0.,1.,0.));
#11714=DIRECTION('ref_axis',(1.,0.,0.));
#11715=DIRECTION('',(0.,-1.,0.));
#11716=DIRECTION('center_axis',(0.,1.,0.));
#11717=DIRECTION('ref_axis',(1.,0.,0.));
#11718=DIRECTION('center_axis',(0.,1.,0.));
#11719=DIRECTION('ref_axis',(1.,0.,0.));
#11720=DIRECTION('center_axis',(0.,1.,0.));
#11721=DIRECTION('ref_axis',(1.,0.,0.));
#11722=DIRECTION('center_axis',(0.,1.,0.));
#11723=DIRECTION('ref_axis',(1.,0.,0.));
#11724=DIRECTION('',(0.,-1.,0.));
#11725=DIRECTION('center_axis',(0.,1.,0.));
#11726=DIRECTION('ref_axis',(1.,0.,0.));
#14744=CARTESIAN_POINT('',(0.,0.,0.));
#14745=CARTESIAN_POINT('Origin',(0.,15.2,3.5));
#14746=CARTESIAN_POINT('',(-0.165,15.2,3.5));
#14747=CARTESIAN_POINT('Origin',(0.,15.2,3.5));
#14748=CARTESIAN_POINT('',(-0.165,16.3,3.5));
#14749=CARTESIAN_POINT('',(-0.165,15.2,3.5));
#14750=CARTESIAN_POINT('Origin',(0.,16.3,3.5));
#14751=CARTESIAN_POINT('Origin',(0.,15.2,3.5));
#14752=CARTESIAN_POINT('Origin',(0.,13.7,3.5));
#14753=CARTESIAN_POINT('',(-0.8,13.7,3.5));
#14754=CARTESIAN_POINT('Origin',(0.,13.7,3.5));
#14755=CARTESIAN_POINT('',(-0.5,13.7,3.5));
#14756=CARTESIAN_POINT('Origin',(0.,13.7,3.5));
#14757=CARTESIAN_POINT('Origin',(0.,13.3,3.5));
#14758=CARTESIAN_POINT('',(-0.8,13.3,3.5));
#14759=CARTESIAN_POINT('',(-0.8,13.3,3.5));
#14760=CARTESIAN_POINT('Origin',(0.,13.3,3.5));
#14761=CARTESIAN_POINT('Origin',(0.,13.3,3.5));
#14762=CARTESIAN_POINT('Origin',(0.,13.7,3.5));
#14763=CARTESIAN_POINT('',(-0.5,16.3,3.5));
#14764=CARTESIAN_POINT('Origin',(0.,16.3,3.5));
#14765=CARTESIAN_POINT('',(-0.5,13.7,3.5));
#14766=CARTESIAN_POINT('Origin',(0.,16.3,3.5));
#16172=UNCERTAINTY_MEASURE_WITH_UNIT(LENGTH_MEASURE(0.001),#16282,
'DISTANCE_ACCURACY_VALUE',
'Maximum model space distance between geometric entities at asserted c
onnectivities');
#16212=UNCERTAINTY_MEASURE_WITH_UNIT(LENGTH_MEASURE(0.001),#16282,
'DISTANCE_ACCURACY_VALUE',
'Maximum model space distance between geometric entities at asserted c
onnectivities');
#16241=(
GEOMETRIC_REPRESENTATION_CONTEXT(3)
GLOBAL_UNCERTAINTY_ASSIGNED_CONTEXT((#16172))
GLOBAL_UNIT_ASSIGNED_CONTEXT((#16282,#16284,#16285))
REPRESENTATION_CONTEXT('','3D')
);
#16281=(
GEOMETRIC_REPRESENTATION_CONTEXT(3)
GLOBAL_UNCERTAINTY_ASSIGNED_CONTEXT((#16212))
GLOBAL_UNIT_ASSIGNED_CONTEXT((#16282,#16284,#16285))
REPRESENTATION_CONTEXT('','3D')
);
#16282=(
LENGTH_UNIT()
NAMED_UNIT(*)
SI_UNIT(.CENTI.,.METRE.)
);
#16284=(
NAMED_UNIT(*)
PLANE_ANGLE_UNIT()
SI_UNIT($,.RADIAN.)
);
#16285=(
NAMED_UNIT(*)
SI_UNIT($,.STERADIAN.)
SOLID_ANGLE_UNIT()
);
#16314=SHAPE_DEFINITION_REPRESENTATION(#16408,#16547);
#16408=PRODUCT_DEFINITION_SHAPE('',$,#16616);
#16547=SHAPE_REPRESENTATION('',(#9645),#16241);
#16587=PRODUCT_DEFINITION_CONTEXT('part definition',#16793,'design');
#16616=PRODUCT_DEFINITION('Roller axle (1)','Roller axle (1)',#16684,#16587);
#16684=PRODUCT_DEFINITION_FORMATION('',$,#16823);
#16793=APPLICATION_CONTEXT(
'Core Data for Automotive Mechanical Design Process');
#16794=PRODUCT_CONTEXT('part definition',#16793,'mechanical');
#16823=PRODUCT('Roller axle (1)','Roller axle (1)','Roller axle (1)',(#16794));
#16926=COLOUR_RGB('Grey',0.48,0.52,0.57);
#16927=FILL_AREA_STYLE_COLOUR('',#16926);
#16928=FILL_AREA_STYLE('',(#16927));
#16929=SURFACE_STYLE_FILL_AREA(#16928);
#16930=SURFACE_SIDE_STYLE('',(#16929));
#16931=SURFACE_STYLE_USAGE(.BOTH.,#16930);
#16932=PRESENTATION_STYLE_ASSIGNMENT((#16931));
ENDSEC;
END-ISO-10303-21;
